ISO-10303-21;
HEADER;
/* Generated by software containing ST-Developer
 * from STEP Tools, Inc. (www.steptools.com) 
 */

FILE_DESCRIPTION(
/* description */ ('Single-Axis Profile-Rail Linear Slide'),
/* implementation_level */ '2;1');

FILE_NAME(
/* name */ 'Flat Washer - M4.step',
/* time_stamp */ '2026-10-27T10:47:43-07:00',
/* author */ (''),
/* organization */ (''),
/* preprocessor_version */ 'ST-DEVELOPER v20.2',
/* originating_system */ 'Autodesk Translation Framework v15.17.0.0',
/* authorisation */ '');

FILE_SCHEMA (('AUTOMOTIVE_DESIGN { 1 0 10303 214 3 1 1 }'));
ENDSEC;

DATA;
#10=MECHANICAL_DESIGN_GEOMETRIC_PRESENTATION_REPRESENTATION('',(#352),#14478);
#254=CONICAL_SURFACE('',#9495,0.225,0.785398163397448);
#298=SHAPE_REPRESENTATION_RELATIONSHIP('SRR','None',#14630,#325);
#325=ADVANCED_BREP_SHAPE_REPRESENTATION('',(#376),#14474);
#352=STYLED_ITEM('',(#14838),#376);
#376=MANIFOLD_SOLID_BREP('Body1',#8615);
#462=FACE_BOUND('',#1794,.T.);
#463=FACE_BOUND('',#1797,.T.);
#814=PLANE('',#9500);
#815=PLANE('',#9504);
#1252=FACE_OUTER_BOUND('',#1791,.T.);
#1253=FACE_OUTER_BOUND('',#1792,.T.);
#1254=FACE_OUTER_BOUND('',#1793,.T.);
#1255=FACE_OUTER_BOUND('',#1795,.T.);
#1256=FACE_OUTER_BOUND('',#1796,.T.);
#1791=EDGE_LOOP('',(#7915,#7916,#7917,#7918));
#1792=EDGE_LOOP('',(#7919,#7920,#7921,#7922));
#1793=EDGE_LOOP('',(#7923));
#1794=EDGE_LOOP('',(#7924));
#1795=EDGE_LOOP('',(#7925,#7926,#7927,#7928));
#1796=EDGE_LOOP('',(#7929));
#1797=EDGE_LOOP('',(#7930));
#2758=LINE('',#14191,#3729);
#2759=LINE('',#14195,#3730);
#2760=LINE('',#14202,#3731);
#3729=VECTOR('',#11695,0.225);
#3730=VECTOR('',#11700,0.215);
#3731=VECTOR('',#11709,0.45);
#3913=CIRCLE('',#9496,0.235);
#3914=CIRCLE('',#9497,0.215);
#3915=CIRCLE('',#9499,0.215);
#3916=CIRCLE('',#9501,0.45);
#3917=CIRCLE('',#9503,0.45);
#4635=VERTEX_POINT('',#14188);
#4636=VERTEX_POINT('',#14190);
#4637=VERTEX_POINT('',#14194);
#4638=VERTEX_POINT('',#14198);
#4639=VERTEX_POINT('',#14201);
#5735=EDGE_CURVE('',#4635,#4635,#3913,.T.);
#5736=EDGE_CURVE('',#4635,#4636,#2758,.T.);
#5737=EDGE_CURVE('',#4636,#4636,#3914,.T.);
#5738=EDGE_CURVE('',#4636,#4637,#2759,.T.);
#5739=EDGE_CURVE('',#4637,#4637,#3915,.T.);
#5740=EDGE_CURVE('',#4638,#4638,#3916,.T.);
#5741=EDGE_CURVE('',#4638,#4639,#2760,.T.);
#5742=EDGE_CURVE('',#4639,#4639,#3917,.T.);
#7915=ORIENTED_EDGE('',*,*,#5735,.T.);
#7916=ORIENTED_EDGE('',*,*,#5736,.T.);
#7917=ORIENTED_EDGE('',*,*,#5737,.T.);
#7918=ORIENTED_EDGE('',*,*,#5736,.F.);
#7919=ORIENTED_EDGE('',*,*,#5737,.F.);
#7920=ORIENTED_EDGE('',*,*,#5738,.T.);
#7921=ORIENTED_EDGE('',*,*,#5739,.T.);
#7922=ORIENTED_EDGE('',*,*,#5738,.F.);
#7923=ORIENTED_EDGE('',*,*,#5740,.T.);
#7924=ORIENTED_EDGE('',*,*,#5735,.F.);
#7925=ORIENTED_EDGE('',*,*,#5740,.F.);
#7926=ORIENTED_EDGE('',*,*,#5741,.T.);
#7927=ORIENTED_EDGE('',*,*,#5742,.T.);
#7928=ORIENTED_EDGE('',*,*,#5741,.F.);
#7929=ORIENTED_EDGE('',*,*,#5742,.F.);
#7930=ORIENTED_EDGE('',*,*,#5739,.F.);
#8126=CYLINDRICAL_SURFACE('',#9498,0.215);
#8127=CYLINDRICAL_SURFACE('',#9502,0.45);
#8546=ADVANCED_FACE('',(#1252),#254,.F.);
#8547=ADVANCED_FACE('',(#1253),#8126,.F.);
#8548=ADVANCED_FACE('',(#1254,#462),#814,.T.);
#8549=ADVANCED_FACE('',(#1255),#8127,.T.);
#8550=ADVANCED_FACE('',(#1256,#463),#815,.F.);
#8615=CLOSED_SHELL('',(#8546,#8547,#8548,#8549,#8550));
#9494=AXIS2_PLACEMENT_3D('',#14186,#11689,#11690);
#9495=AXIS2_PLACEMENT_3D('',#14187,#11691,#11692);
#9496=AXIS2_PLACEMENT_3D('',#14189,#11693,#11694);
#9497=AXIS2_PLACEMENT_3D('',#14192,#11696,#11697);
#9498=AXIS2_PLACEMENT_3D('',#14193,#11698,#11699);
#9499=AXIS2_PLACEMENT_3D('',#14196,#11701,#11702);
#9500=AXIS2_PLACEMENT_3D('',#14197,#11703,#11704);
#9501=AXIS2_PLACEMENT_3D('',#14199,#11705,#11706);
#9502=AXIS2_PLACEMENT_3D('',#14200,#11707,#11708);
#9503=AXIS2_PLACEMENT_3D('',#14203,#11710,#11711);
#9504=AXIS2_PLACEMENT_3D('',#14204,#11712,#11713);
#11689=DIRECTION('axis',(0.,0.,1.));
#11690=DIRECTION('refdir',(1.,0.,0.));
#11691=DIRECTION('center_axis',(0.,1.,0.));
#11692=DIRECTION('ref_axis',(1.,0.,0.));
#11693=DIRECTION('center_axis',(0.,1.,0.));
#11694=DIRECTION('ref_axis',(1.,0.,0.));
#11695=DIRECTION('',(0.707106781186547,-0.707106781186548,-8.65956056235493E-17));
#11696=DIRECTION('center_axis',(0.,-1.,0.));
#11697=DIRECTION('ref_axis',(1.,0.,0.));
#11698=DIRECTION('center_axis',(0.,1.,0.));
#11699=DIRECTION('ref_axis',(1.,0.,0.));
#11700=DIRECTION('',(0.,-1.,0.));
#11701=DIRECTION('center_axis',(0.,-1.,0.));
#11702=DIRECTION('ref_axis',(1.,0.,0.));
#11703=DIRECTION('center_axis',(0.,1.,0.));
#11704=DIRECTION('ref_axis',(1.,0.,0.));
#11705=DIRECTION('center_axis',(0.,1.,0.));
#11706=DIRECTION('ref_axis',(1.,0.,0.));
#11707=DIRECTION('center_axis',(0.,1.,0.));
#11708=DIRECTION('ref_axis',(1.,0.,0.));
#11709=DIRECTION('',(0.,-1.,0.));
#11710=DIRECTION('center_axis',(0.,1.,0.));
#11711=DIRECTION('ref_axis',(1.,0.,0.));
#11712=DIRECTION('center_axis',(0.,1.,0.));
#11713=DIRECTION('ref_axis',(1.,0.,0.));
#14186=CARTESIAN_POINT('',(0.,0.,0.));
#14187=CARTESIAN_POINT('Origin',(0.,0.07,0.));
#14188=CARTESIAN_POINT('',(-0.235,0.08,2.87791997799628E-17));
#14189=CARTESIAN_POINT('Origin',(0.,0.08,0.));
#14190=CARTESIAN_POINT('',(-0.215,0.06,-2.63299061816681E-17));
#14191=CARTESIAN_POINT('',(-0.225,0.07,2.75545529808154E-17));
#14192=CARTESIAN_POINT('Origin',(0.,0.06,0.));
#14193=CARTESIAN_POINT('Origin',(0.,0.,0.));
#14194=CARTESIAN_POINT('',(-0.215,0.,2.63299061816681E-17));
#14195=CARTESIAN_POINT('',(-0.215,0.,2.63299061816681E-17));
#14196=CARTESIAN_POINT('Origin',(0.,0.,0.));
#14197=CARTESIAN_POINT('Origin',(0.,0.08,0.));
#14198=CARTESIAN_POINT('',(-0.45,0.08,5.51091059616309E-17));
#14199=CARTESIAN_POINT('Origin',(0.,0.08,0.));
#14200=CARTESIAN_POINT('Origin',(0.,0.,0.));
#14201=CARTESIAN_POINT('',(-0.45,0.,5.51091059616309E-17));
#14202=CARTESIAN_POINT('',(-0.45,0.,5.51091059616309E-17));
#14203=CARTESIAN_POINT('Origin',(0.,0.,0.));
#14204=CARTESIAN_POINT('Origin',(0.,0.,0.));
#14442=UNCERTAINTY_MEASURE_WITH_UNIT(LENGTH_MEASURE(0.001),#14479,
'DISTANCE_ACCURACY_VALUE',
'Maximum model space distance between geometric entities at asserted c
onnectivities');
#14446=UNCERTAINTY_MEASURE_WITH_UNIT(LENGTH_MEASURE(0.001),#14479,
'DISTANCE_ACCURACY_VALUE',
'Maximum model space distance between geometric entities at asserted c
onnectivities');
#14474=(
GEOMETRIC_REPRESENTATION_CONTEXT(3)
GLOBAL_UNCERTAINTY_ASSIGNED_CONTEXT((#14442))
GLOBAL_UNIT_ASSIGNED_CONTEXT((#14479,#14481,#14482))
REPRESENTATION_CONTEXT('','3D')
);
#14478=(
GEOMETRIC_REPRESENTATION_CONTEXT(3)
GLOBAL_UNCERTAINTY_ASSIGNED_CONTEXT((#14446))
GLOBAL_UNIT_ASSIGNED_CONTEXT((#14479,#14481,#14482))
REPRESENTATION_CONTEXT('','3D')
);
#14479=(
LENGTH_UNIT()
NAMED_UNIT(*)
SI_UNIT(.CENTI.,.METRE.)
);
#14481=(
NAMED_UNIT(*)
PLANE_ANGLE_UNIT()
SI_UNIT($,.RADIAN.)
);
#14482=(
NAMED_UNIT(*)
SI_UNIT($,.STERADIAN.)
SOLID_ANGLE_UNIT()
);
#14510=SHAPE_DEFINITION_REPRESENTATION(#14544,#14630);
#14544=PRODUCT_DEFINITION_SHAPE('',$,#14662);
#14630=SHAPE_REPRESENTATION('',(#9494),#14474);
#14634=PRODUCT_DEFINITION_CONTEXT('part definition',#14729,'design');
#14662=PRODUCT_DEFINITION('Flat Washer - M4','Flat Washer - M4',#14693,
#14634);
#14693=PRODUCT_DEFINITION_FORMATION('',$,#14758);
#14729=APPLICATION_CONTEXT(
'Core Data for Automotive Mechanical Design Process');
#14730=PRODUCT_CONTEXT('part definition',#14729,'mechanical');
#14758=PRODUCT('Flat Washer - M4','Flat Washer - M4','Flat Washer - M4',
(#14730));
#14832=COLOUR_RGB('Black',0.12,0.14,0.17);
#14833=FILL_AREA_STYLE_COLOUR('',#14832);
#14834=FILL_AREA_STYLE('',(#14833));
#14835=SURFACE_STYLE_FILL_AREA(#14834);
#14836=SURFACE_SIDE_STYLE('',(#14835));
#14837=SURFACE_STYLE_USAGE(.BOTH.,#14836);
#14838=PRESENTATION_STYLE_ASSIGNMENT((#14837));
ENDSEC;
END-ISO-10303-21;
